ISO-10303-21;
HEADER;
FILE_DESCRIPTION (('STEP AP214'),
    '1' );
FILE_NAME ('socket button head screw_iso_ISO 7380 - M5 x 16 - 16C.step',
    '2026-09-24T10:15:42',
    ( '' ),
    ( '' ),
    'SwSTEP 2.0',
    'SolidWorks 2026',
    '' );
FILE_SCHEMA (( 'AUTOMOTIVE_DESIGN' ));
ENDSEC;

DATA;
#29=DIRECTION ( 'NONE',  ( -1.000000000000000000, -0.000000000000000000, -0.000000000000000000 ) ) ;
#36=ORIENTED_EDGE ( 'NONE', *, *, #16394, .F. ) ;
#43=DIRECTION ( 'NONE',  ( -1.000000000000000000, -0.000000000000000000, -0.000000000000000000 ) ) ;
#47=LINE ( 'NONE', #1670, #13971 ) ;
#54=AXIS2_PLACEMENT_3D ( 'NONE', #4201, #10016, #14696 ) ;
#57=ORIENTED_EDGE ( 'NONE', *, *, #11432, .T. ) ;
#120=DIRECTION ( 'NONE',  ( -1.000000000000000000, 0.000000000000000000, 0.000000000000000000 ) ) ;
#130=EDGE_CURVE ( 'NONE', #2733, #15610, #8916, .T. ) ;
#170=DIRECTION ( 'NONE',  ( 0.000000000000000000, 0.000000000000000000, 1.000000000000000000 ) ) ;
#173=DIRECTION ( 'NONE',  ( -0.000000000000000000, -1.000000000000000000, -0.000000000000000000 ) ) ;
#193=LINE ( 'NONE', #2016, #8413 ) ;
#205=CARTESIAN_POINT ( 'NONE',  ( 0.000000000000000000, -0.8660254037844384856, -1.500000000000000000 ) ) ;
#261=AXIS2_PLACEMENT_3D ( 'NONE', #3469, #7605, #6250 ) ;
#294=ADVANCED_FACE ( 'NONE', ( #16576 ), #10453, .T. ) ;
#314=ORIENTED_EDGE ( 'NONE', *, *, #12569, .F. ) ;
#315=ADVANCED_FACE ( 'NONE', ( #16942 ), #17658, .F. ) ;
#327=ORIENTED_EDGE ( 'NONE', *, *, #6533, .F. ) ;
#337=DIRECTION ( 'NONE',  ( 0.000000000000000000, 0.5000000000000003331, -0.8660254037844383745 ) ) ;
#401=LINE ( 'NONE', #4898, #14257 ) ;
#480=DIRECTION ( 'NONE',  ( 0.000000000000000000, 1.000000000000000000, 0.000000000000000000 ) ) ;
#507=CARTESIAN_POINT ( 'NONE',  ( 1.560000000000000053, 1.299038105676658228, 0.7500000000000009992 ) ) ;
#567=EDGE_CURVE ( 'NONE', #18684, #10257, #1633, .T. ) ;
#603=DIRECTION ( 'NONE',  ( -0.5000000000000042188, 0.000000000000000000, 0.8660254037844361541 ) ) ;
#607=( LENGTH_UNIT ( ) NAMED_UNIT ( * ) SI_UNIT ( .MILLI., .METRE. ) );
#609=CARTESIAN_POINT ( 'NONE',  ( 1.560000000000000053, 0.8660254037844389297, -1.500000000000000000 ) ) ;
#658=ORIENTED_EDGE ( 'NONE', *, *, #9985, .F. ) ;
#661=VECTOR ( 'NONE', #6476, 1000.000000000000000 ) ;
#665=CARTESIAN_POINT ( 'NONE',  ( 18.75000000000000000, 2.789133085058096608E-16, -2.055000000000000160 ) ) ;
#680=EDGE_CURVE ( 'NONE', #4361, #18405, #6716, .T. ) ;
#694=( NAMED_UNIT ( * ) SI_UNIT ( $, .STERADIAN. ) SOLID_ANGLE_UNIT ( ) );
#818=ORIENTED_EDGE ( 'NONE', *, *, #17943, .F. ) ;
#844=PLANE ( 'NONE',  #12960 ) ;
#951=EDGE_CURVE ( 'NONE', #11815, #17865, #15847, .T. ) ;
#1049=AXIS2_PLACEMENT_3D ( 'NONE', #1810, #12037, #17872 ) ;
#1082=LINE ( 'NONE', #2506, #14552 ) ;
#1084=ORIENTED_EDGE ( 'NONE', *, *, #2353, .T. ) ;
#1087=VERTEX_POINT ( 'NONE', #8024 ) ;
#1093=FACE_OUTER_BOUND ( 'NONE', #18260, .T. ) ;
#1098=EDGE_CURVE ( 'NONE', #18405, #4361, #3805, .T. ) ;
#1101=ORIENTED_EDGE ( 'NONE', *, *, #3756, .F. ) ;
#1128=CARTESIAN_POINT ( 'NONE',  ( 2.949999999999999734, 0.000000000000000000, 0.000000000000000000 ) ) ;
#1137=VERTEX_POINT ( 'NONE', #12404 ) ;
#1204=EDGE_LOOP ( 'NONE', ( #8182, #16614, #818 ) ) ;
#1223=ORIENTED_EDGE ( 'NONE', *, *, #12186, .F. ) ;
#1269=ORIENTED_EDGE ( 'NONE', *, *, #10296, .F. ) ;
#1286=ADVANCED_FACE ( 'NONE', ( #11626 ), #2628, .T. ) ;
#1288=ADVANCED_FACE ( 'NONE', ( #11347 ), #1322, .F. ) ;
#1313=DIRECTION ( 'NONE',  ( 0.000000000000000000, 0.000000000000000000, 1.000000000000000000 ) ) ;
#1321=AXIS2_PLACEMENT_3D ( 'NONE', #17112, #8244, #5361 ) ;
#1322=TOROIDAL_SURFACE ( 'NONE', #12022, 2.699999999999999734, 0.2000000000000000111 ) ;
#1345=CARTESIAN_POINT ( 'NONE',  ( 2.369999999999999662, 4.749999999999999112, 0.000000000000000000 ) ) ;
#1360=DIRECTION ( 'NONE',  ( -1.000000000000000000, -0.000000000000000000, -0.000000000000000000 ) ) ;
#1418=ORIENTED_EDGE ( 'NONE', *, *, #13120, .F. ) ;
#1461=CARTESIAN_POINT ( 'NONE',  ( 2.369999999999999662, 0.000000000000000000, 0.000000000000000000 ) ) ;
#1464=PLANE ( 'NONE',  #11429 ) ;
#1469=EDGE_LOOP ( 'NONE', ( #658, #13216, #16191 ) ) ;
#1552=LINE ( 'NONE', #13303, #15949 ) ;
#1555=LINE ( 'NONE', #16380, #4099 ) ;
#1617=ADVANCED_FACE ( 'NONE', ( #8525 ), #2063, .F. ) ;
#1626=DIRECTION ( 'NONE',  ( -1.000000000000000000, -0.000000000000000000, -0.000000000000000000 ) ) ;
#1633=LINE ( 'NONE', #205, #6254 ) ;
#1659=EDGE_CURVE ( 'NONE', #11688, #11324, #401, .T. ) ;
#1670=CARTESIAN_POINT ( 'NONE',  ( 1.560000000000000053, 0.8660254037844389297, 1.500000000000000000 ) ) ;
#1761=ORIENTED_EDGE ( 'NONE', *, *, #7020, .T. ) ;
#1790=EDGE_CURVE ( 'NONE', #2855, #2106, #2387, .T. ) ;
#1810=CARTESIAN_POINT ( 'NONE',  ( 0.000000000000000000, 0.000000000000000000, 0.000000000000000000 ) ) ;
#1849=CARTESIAN_POINT ( 'NONE',  ( 2.750000000000000000, 0.000000000000000000, 0.000000000000000000 ) ) ;
#1936=VERTEX_POINT ( 'NONE', #10025 ) ;
#1943=CIRCLE ( 'NONE', #13220, 2.699999999999999734 ) ;
#1975=EDGE_CURVE ( 'NONE', #11815, #11886, #5621, .T. ) ;
#1988=CARTESIAN_POINT ( 'NONE',  ( 1.560000000000000053, -0.8660254037844384856, -1.500000000000000000 ) ) ;
#1990=CARTESIAN_POINT ( 'NONE',  ( 0.000000000000000000, 0.000000000000000000, 0.000000000000000000 ) ) ;
#2003=EDGE_LOOP ( 'NONE', ( #7026, #3592, #14579 ) ) ;
#2016=CARTESIAN_POINT ( 'NONE',  ( 18.75000000000000000, 2.516649172247811061E-16, -2.055000000000000160 ) ) ;
#2028=VECTOR ( 'NONE', #14678, 1000.000000000000000 ) ;
#2030=AXIS2_PLACEMENT_3D ( 'NONE', #15716, #11248, #17249 ) ;
#2063=CONICAL_SURFACE ( 'NONE', #15181, 1732.050807568857181, 1.047197551196592746 ) ;
#2073=PRODUCT_DEFINITION ( 'UNKNOWN', '', #9290, #10776 ) ;
#2098=ORIENTED_EDGE ( 'NONE', *, *, #10946, .T. ) ;
#2100=CARTESIAN_POINT ( 'NONE',  ( 1.560000000000000053, 1.299038105676658228, -0.7500000000000009992 ) ) ;
#2106=VERTEX_POINT ( 'NONE', #9540 ) ;
#2135=DIRECTION ( 'NONE',  ( -1.000000000000000000, -0.000000000000000000, -0.000000000000000000 ) ) ;
#2138=DIRECTION ( 'NONE',  ( 0.000000000000000000, 0.000000000000000000, 1.000000000000000000 ) ) ;
#2180=ORIENTED_EDGE ( 'NONE', *, *, #9576, .T. ) ;
#2188=FACE_OUTER_BOUND ( 'NONE', #16097, .T. ) ;
#2233=CARTESIAN_POINT ( 'NONE',  ( 1.560000000000000053, 0.8660254037844389297, -1.500000000000000000 ) ) ;
#2259=CIRCLE ( 'NONE', #11127, 2.055000000000000160 ) ;
#2303=DIRECTION ( 'NONE',  ( 0.000000000000000000, 0.8660254037844384856, 0.5000000000000004441 ) ) ;
#2342=VECTOR ( 'NONE', #15238, 999.9999999999998863 ) ;
#2353=EDGE_CURVE ( 'NONE', #5495, #10362, #16219, .T. ) ;
#2376=ORIENTED_EDGE ( 'NONE', *, *, #1659, .T. ) ;
#2378=DIRECTION ( 'NONE',  ( 0.000000000000000000, 0.000000000000000000, 1.000000000000000000 ) ) ;
#2387=LINE ( 'NONE', #15298, #17614 ) ;
#2448=( LENGTH_UNIT ( ) NAMED_UNIT ( * ) SI_UNIT ( .MILLI., .METRE. ) );
#2452=CARTESIAN_POINT ( 'NONE',  ( 1.560000000000000053, -1.732050807568877859, -1.752539433813135784E-17 ) ) ;
#2506=CARTESIAN_POINT ( 'NONE',  ( 1.560000000000000053, -0.8660254037844384856, 1.500000000000000000 ) ) ;
#2531=DIRECTION ( 'NONE',  ( 0.000000000000000000, 0.000000000000000000, 1.000000000000000000 ) ) ;
#2617=FACE_OUTER_BOUND ( 'NONE', #13214, .T. ) ;
#2628=CYLINDRICAL_SURFACE ( 'NONE', #16295, 4.750000000000000000 ) ;
#2668=FACE_OUTER_BOUND ( 'NONE', #4674, .T. ) ;
#2671=AXIS2_PLACEMENT_3D ( 'NONE', #1128, #7154, #1313 ) ;
#2679=EDGE_CURVE ( 'NONE', #12041, #1137, #12547, .T. ) ;
#2697=ORIENTED_EDGE ( 'NONE', *, *, #9796, .T. ) ;
#2698=CARTESIAN_POINT ( 'NONE',  ( 1.560000000000000053, 0.8660254037844389297, -1.500000000000000000 ) ) ;
#2702=ORIENTED_EDGE ( 'NONE', *, *, #14408, .F. ) ;
#2733=VERTEX_POINT ( 'NONE', #16767 ) ;
#2764=ORIENTED_EDGE ( 'NONE', *, *, #5105, .T. ) ;
#2771=CIRCLE ( 'NONE', #9508, 4.750000000000000000 ) ;
#2791=AXIS2_PLACEMENT_3D ( 'NONE', #5044, #7742, #9450 ) ;
#2798=DIRECTION ( 'NONE',  ( -1.000000000000000000, 0.000000000000000000, 0.000000000000000000 ) ) ;
#2855=VERTEX_POINT ( 'NONE', #14354 ) ;
#2860=DIRECTION ( 'NONE',  ( -1.000000000000000000, -0.000000000000000000, -0.000000000000000000 ) ) ;
#2910=CARTESIAN_POINT ( 'NONE',  ( 1.560000000000000053, 0.000000000000000000, 0.000000000000000000 ) ) ;
#2912=FACE_OUTER_BOUND ( 'NONE', #1204, .T. ) ;
#2971=DIRECTION ( 'NONE',  ( -1.000000000000000000, 0.000000000000000000, 0.000000000000000000 ) ) ;
#2995=ORIENTED_EDGE ( 'NONE', *, *, #680, .F. ) ;
#3036=CARTESIAN_POINT ( 'NONE',  ( 2.949999999999999734, 3.061616997868382648E-16, -2.499999999999999556 ) ) ;
#3109=EDGE_CURVE ( 'NONE', #6836, #6081, #11271, .T. ) ;
#3110=FACE_OUTER_BOUND ( 'NONE', #7738, .T. ) ;
#3114=EDGE_CURVE ( 'NONE', #11324, #13735, #3993, .T. ) ;
#3118=ORIENTED_EDGE ( 'NONE', *, *, #12569, .T. ) ;
#3137=ORIENTED_EDGE ( 'NONE', *, *, #15735, .T. ) ;
#3140=VERTEX_POINT ( 'NONE', #2452 ) ;
#3218=ORIENTED_EDGE ( 'NONE', *, *, #8590, .T. ) ;
#3222=DIRECTION ( 'NONE',  ( 0.000000000000000000, 0.000000000000000000, 1.000000000000000000 ) ) ;
#3324=CYLINDRICAL_SURFACE ( 'NONE', #1049, 2.499999999999999556 ) ;
#3358=FILL_AREA_STYLE ('',( #5079 ) ) ;
#3418=ORIENTED_EDGE ( 'NONE', *, *, #4040, .F. ) ;
#3452=DIRECTION ( 'NONE',  ( -1.000000000000000000, 0.000000000000000000, -0.000000000000000000 ) ) ;
#3469=CARTESIAN_POINT ( 'NONE',  ( 1.560000000000000053, 0.000000000000000000, 2.999999999999998668 ) ) ;
#3515=VECTOR ( 'NONE', #603, 1000.000000000000114 ) ;
#3524=CARTESIAN_POINT ( 'NONE',  ( 0.000000000000000000, -0.8660254037844384856, 1.500000000000000000 ) ) ;
#3566=CIRCLE ( 'NONE', #14248, 4.750000000000000000 ) ;
#3585=DIRECTION ( 'NONE',  ( 0.000000000000000000, 0.000000000000000000, 1.000000000000000000 ) ) ;
#3592=ORIENTED_EDGE ( 'NONE', *, *, #3109, .F. ) ;
#3594=EDGE_LOOP ( 'NONE', ( #1084, #6237, #8896, #16235, #12973 ) ) ;
#3637=VERTEX_POINT ( 'NONE', #3945 ) ;
#3644=CARTESIAN_POINT ( 'NONE',  ( 1.560000000000000053, -0.8660254037844384856, 1.500000000000000000 ) ) ;
#3662=DIRECTION ( 'NONE',  ( -1.000000000000000000, -0.000000000000000000, -0.000000000000000000 ) ) ;
#3725=CIRCLE ( 'NONE', #54, 2.499999999999999556 ) ;
#3756=EDGE_CURVE ( 'NONE', #12041, #8377, #13099, .T. ) ;
#3781=DIRECTION ( 'NONE',  ( -1.000000000000000000, 0.000000000000000000, -0.000000000000000000 ) ) ;
#3794=ORIENTED_EDGE ( 'NONE', *, *, #11640, .F. ) ;
#3799=PRESENTATION_STYLE_ASSIGNMENT (( #9723 ) ) ;
#3805=CIRCLE ( 'NONE', #8683, 2.375000000000000444 ) ;
#3819=AXIS2_PLACEMENT_3D ( 'NONE', #7749, #15092, #480 ) ;
#3852=FACE_OUTER_BOUND ( 'NONE', #6088, .T. ) ;
#3865=EDGE_CURVE ( 'NONE', #10362, #17016, #8830, .T. ) ;
#3896=CARTESIAN_POINT ( 'NONE',  ( 1.560000000000000053, 1.732050807568878747, 7.017607234860990640E-28 ) ) ;
#3921=ORIENTED_EDGE ( 'NONE', *, *, #18762, .T. ) ;
#3925=LINE ( 'NONE', #9749, #13599 ) ;
#3934=ORIENTED_EDGE ( 'NONE', *, *, #9260, .F. ) ;
#3945=CARTESIAN_POINT ( 'NONE',  ( 18.30499999999999972, 3.061616997868382648E-16, -2.499999999999999556 ) ) ;
#3947=AXIS2_PLACEMENT_3D ( 'NONE', #7345, #5886, #11920 ) ;
#3993=LINE ( 'NONE', #18333, #15180 ) ;
#3998=ORIENTED_EDGE ( 'NONE', *, *, #15156, .T. ) ;
#4040=EDGE_CURVE ( 'NONE', #15271, #15610, #12892, .T. ) ;
#4082=DIRECTION ( 'NONE',  ( 0.000000000000000000, 0.000000000000000000, 1.000000000000000000 ) ) ;
#4099=VECTOR ( 'NONE', #2971, 1000.000000000000000 ) ;
#4165=CARTESIAN_POINT ( 'NONE',  ( 1.560000000000000053, 0.000000000000000000, 2.999999999999998668 ) ) ;
#4201=CARTESIAN_POINT ( 'NONE',  ( 18.30499999999999972, 0.000000000000000000, 0.000000000000000000 ) ) ;
#4222=EDGE_LOOP ( 'NONE', ( #17056, #11964, #9426, #8154, #7583 ) ) ;
#4230=DIRECTION ( 'NONE',  ( -1.000000000000000000, -0.000000000000000000, -0.000000000000000000 ) ) ;
#4251=ORIENTED_EDGE ( 'NONE', *, *, #17943, .T. ) ;
#4300=DIRECTION ( 'NONE',  ( -0.5000000000000042188, 1.060575238724903710E-16, -0.8660254037844361541 ) ) ;
#4313=LINE ( 'NONE', #10138, #11826 ) ;
#4333=DIRECTION ( 'NONE',  ( -0.000000000000000000, -1.000000000000000000, -0.000000000000000000 ) ) ;
#4361=VERTEX_POINT ( 'NONE', #13842 ) ;
#4398=CARTESIAN_POINT ( 'NONE',  ( 0.000000000000000000, 0.000000000000000000, 2.499999999999999556 ) ) ;
#4417=EDGE_CURVE ( 'NONE', #6836, #15610, #14148, .T. ) ;
#4426=AXIS2_PLACEMENT_3D ( 'NONE', #13422, #43, #4639 ) ;
#4473=PLANE ( 'NONE',  #15293 ) ;
#4477=PRODUCT ( 'socket button head screw_iso_ISO 7380 - M5 x 16 - 16C', 'socket button head screw_iso_ISO 7380 - M5 x 16 - 16C', '', ( #18110 ) ) ;
#4478=SHAPE_REPRESENTATION ( 'socket button head screw_iso_ISO 7380 - M5 x 16 - 16C', ( #2030 ), #16378 ) ;
#4494=DIRECTION ( 'NONE',  ( 0.000000000000000000, -1.224646799147353207E-16, 1.000000000000000000 ) ) ;
#4503=ORIENTED_EDGE ( 'NONE', *, *, #6801, .F. ) ;
#4515=DIRECTION ( 'NONE',  ( 0.000000000000000000, 0.000000000000000000, 1.000000000000000000 ) ) ;
#4534=ORIENTED_EDGE ( 'NONE', *, *, #3756, .T. ) ;
#4550=LINE ( 'NONE', #16112, #12136 ) ;
#4634=EDGE_CURVE ( 'NONE', #8377, #12041, #2259, .T. ) ;
#4639=DIRECTION ( 'NONE',  ( 0.000000000000000000, 0.000000000000000000, 1.000000000000000000 ) ) ;
#4674=EDGE_LOOP ( 'NONE', ( #6178, #16124, #36 ) ) ;
#4703=ORIENTED_EDGE ( 'NONE', *, *, #4417, .F. ) ;
#4733=CARTESIAN_POINT ( 'NONE',  ( 0.000000000000000000, -0.8660254037844384856, -1.500000000000000000 ) ) ;
#4734=VECTOR ( 'NONE', #13350, 1000.000000000000000 ) ;
#4751=VECTOR ( 'NONE', #173, 1000.000000000000000 ) ;
#4754=CARTESIAN_POINT ( 'NONE',  ( 18.75000000000000000, 0.000000000000000000, 0.000000000000000000 ) ) ;
#4756=DIRECTION ( 'NONE',  ( -1.000000000000000000, -0.000000000000000000, -0.000000000000000000 ) ) ;
#4851=DIRECTION ( 'NONE',  ( 0.000000000000000000, 0.000000000000000000, 1.000000000000000000 ) ) ;
#4898=CARTESIAN_POINT ( 'NONE',  ( 1.560000000000000053, 0.8660254037844389297, -1.500000000000000000 ) ) ;
#4901=DIRECTION ( 'NONE',  ( 0.000000000000000000, 0.000000000000000000, -1.000000000000000000 ) ) ;
#4959=DIRECTION ( 'NONE',  ( 0.000000000000000000, 0.000000000000000000, 1.000000000000000000 ) ) ;
#5040=EDGE_LOOP ( 'NONE', ( #18194, #6987, #15036, #3794 ) ) ;
#5044=CARTESIAN_POINT ( 'NONE',  ( 4.755015822784811164, -4.336808689942017736E-16, 0.000000000000000000 ) ) ;
#5079=FILL_AREA_STYLE_COLOUR ( '', #12704 ) ;
#5091=ORIENTED_EDGE ( 'NONE', *, *, #6885, .F. ) ;
#5103=DIRECTION ( 'NONE',  ( -1.000000000000000000, 0.000000000000000000, 0.000000000000000000 ) ) ;
#5105=EDGE_CURVE ( 'NONE', #5495, #12765, #1555, .T. ) ;
#5152=DIRECTION ( 'NONE',  ( -1.000000000000000000, -0.000000000000000000, -0.000000000000000000 ) ) ;
#5171=ADVANCED_FACE ( 'NONE', ( #16179 ), #1464, .F. ) ;
#5196=SHAPE_DEFINITION_REPRESENTATION ( #6483, #4478 ) ;
#5248=CARTESIAN_POINT ( 'NONE',  ( 2.369999999999999662, 0.000000000000000000, 0.000000000000000000 ) ) ;
#5251=CIRCLE ( 'NONE', #2791, 5.315148208181396328 ) ;
#5270=AXIS2_PLACEMENT_3D ( 'NONE', #7177, #5288, #18822 ) ;
#5287=ADVANCED_FACE ( 'NONE', ( #2668 ), #6996, .T. ) ;
#5288=DIRECTION ( 'NONE',  ( -1.000000000000000000, -0.000000000000000000, -0.000000000000000000 ) ) ;
#5322=DIRECTION ( 'NONE',  ( 0.000000000000000000, 0.8660254037844384856, -0.5000000000000004441 ) ) ;
#5361=DIRECTION ( 'NONE',  ( 0.000000000000000000, 0.000000000000000000, -1.000000000000000000 ) ) ;
#5414=CARTESIAN_POINT ( 'NONE',  ( 2.949999999999999734, 0.000000000000000000, 0.000000000000000000 ) ) ;
#5454=ORIENTED_EDGE ( 'NONE', *, *, #4040, .T. ) ;
#5495=VERTEX_POINT ( 'NONE', #8888 ) ;
#5499=CARTESIAN_POINT ( 'NONE',  ( 0.000000000000000000, 0.000000000000000000, 0.000000000000000000 ) ) ;
#5521=EDGE_CURVE ( 'NONE', #1137, #1087, #6032, .T. ) ;
#5533=CARTESIAN_POINT ( 'NONE',  ( 1.560000000000000053, 0.8660254037844389297, -1.500000000000000000 ) ) ;
#5538=CARTESIAN_POINT ( 'NONE',  ( 1.560000000000000053, 0.000000000000000000, -1.499999999999999556 ) ) ;
#5550=FACE_OUTER_BOUND ( 'NONE', #18681, .T. ) ;
#5562=ORIENTED_EDGE ( 'NONE', *, *, #16833, .F. ) ;
#5569=CIRCLE ( 'NONE', #8047, 4.750000000000000000 ) ;
#5620=DIRECTION ( 'NONE',  ( -0.000000000000000000, -0.5000000000000003331, -0.8660254037844384856 ) ) ;
#5621=CIRCLE ( 'NONE', #16335, 0.2000000000000000944 ) ;
#5641=DIRECTION ( 'NONE',  ( 1.000000000000000000, 0.000000000000000000, 0.000000000000000000 ) ) ;
#5684=APPLICATION_CONTEXT ( 'automotive_design' ) ;
#5726=CARTESIAN_POINT ( 'NONE',  ( 4.755015822784811164, -4.336808689942017736E-16, 0.000000000000000000 ) ) ;
#5747=EDGE_CURVE ( 'NONE', #17499, #1936, #3566, .T. ) ;
#5750=LINE ( 'NONE', #13124, #10278 ) ;
#5762=CARTESIAN_POINT ( 'NONE',  ( 1.560000000000000053, 1.732050807568878747, 7.017607234860990640E-28 ) ) ;
#5821=FACE_OUTER_BOUND ( 'NONE', #16597, .T. ) ;
#5867=DIRECTION ( 'NONE',  ( -0.000000000000000000, -0.5000000000000004441, 0.8660254037844383745 ) ) ;
#5886=DIRECTION ( 'NONE',  ( -1.000000000000000000, 0.000000000000000000, 0.000000000000000000 ) ) ;
#5894=EDGE_LOOP ( 'NONE', ( #314, #13600, #6404, #15748 ) ) ;
#5916=VERTEX_POINT ( 'NONE', #10959 ) ;
#5949=AXIS2_PLACEMENT_3D ( 'NONE', #18581, #13229, #337 ) ;
#5990=DIRECTION ( 'NONE',  ( -1.000000000000000000, -0.000000000000000000, -0.000000000000000000 ) ) ;
#6032=LINE ( 'NONE', #4398, #17935 ) ;
#6033=EDGE_LOOP ( 'NONE', ( #15992, #14556 ) ) ;
#6035=EDGE_CURVE ( 'NONE', #10362, #2855, #1082, .T. ) ;
#6048=CIRCLE ( 'NONE', #2671, 2.499999999999999556 ) ;
#6064=EDGE_LOOP ( 'NONE', ( #12244, #10378, #10510, #4503 ) ) ;
#6081=VERTEX_POINT ( 'NONE', #13122 ) ;
#6088=EDGE_LOOP ( 'NONE', ( #7357, #3934, #4703 ) ) ;
#6131=EDGE_LOOP ( 'NONE', ( #3921, #2697, #16691, #7739, #9158, #3218 ) ) ;
#6147=CARTESIAN_POINT ( 'NONE',  ( 2.369999999999999662, 0.000000000000000000, 0.000000000000000000 ) ) ;
#6178=ORIENTED_EDGE ( 'NONE', *, *, #130, .F. ) ;
#6237=ORIENTED_EDGE ( 'NONE', *, *, #6035, .T. ) ;
#6250=DIRECTION ( 'NONE',  ( 0.000000000000000000, 0.000000000000000000, 1.000000000000000000 ) ) ;
#6254=VECTOR ( 'NONE', #16165, 1000.000000000000114 ) ;
#6344=( NAMED_UNIT ( * ) SI_UNIT ( $, .STERADIAN. ) SOLID_ANGLE_UNIT ( ) );
#6372=CARTESIAN_POINT ( 'NONE',  ( 2.750000000000000000, 0.000000000000000000, 0.000000000000000000 ) ) ;
#6373=CARTESIAN_POINT ( 'NONE',  ( 18.30499999999999972, 0.000000000000000000, 0.000000000000000000 ) ) ;
#6395=VERTEX_POINT ( 'NONE', #1345 ) ;
#6404=ORIENTED_EDGE ( 'NONE', *, *, #5521, .T. ) ;
#6405=AXIS2_PLACEMENT_3D ( 'NONE', #7679, #17711, #14922 ) ;
#6430=LINE ( 'NONE', #12341, #3515 ) ;
#6476=DIRECTION ( 'NONE',  ( -1.000000000000000000, 0.000000000000000000, 0.000000000000000000 ) ) ;
#6477=CYLINDRICAL_SURFACE ( 'NONE', #9623, 2.499999999999999556 ) ;
#6483=PRODUCT_DEFINITION_SHAPE ( 'NONE', 'NONE',  #2073 ) ;
#6502=DIRECTION ( 'NONE',  ( -0.7071067811865486830, 8.659560562354921765E-17, -0.7071067811865464625 ) ) ;
#6533=EDGE_CURVE ( 'NONE', #13259, #17499, #16363, .T. ) ;
#6539=DIRECTION ( 'NONE',  ( 0.000000000000000000, 0.000000000000000000, 1.000000000000000000 ) ) ;
#6607=DIRECTION ( 'NONE',  ( -1.000000000000000000, -0.000000000000000000, -0.000000000000000000 ) ) ;
#6653=DIRECTION ( 'NONE',  ( -1.000000000000000000, -0.000000000000000000, -0.000000000000000000 ) ) ;
#6666=FACE_OUTER_BOUND ( 'NONE', #18433, .T. ) ;
#6716=CIRCLE ( 'NONE', #18902, 2.375000000000000444 ) ;
#6745=AXIS2_PLACEMENT_3D ( 'NONE', #11589, #5641, #9953 ) ;
#6791=CARTESIAN_POINT ( 'NONE',  ( 0.000000000000000000, 0.000000000000000000, 0.000000000000000000 ) ) ;
#6801=EDGE_CURVE ( 'NONE', #3637, #1137, #3725, .T. ) ;
#6836=VERTEX_POINT ( 'NONE', #2100 ) ;
#6872=AXIS2_PLACEMENT_3D ( 'NONE', #9683, #5103, #16766 ) ;
#6883=EDGE_LOOP ( 'NONE', ( #16436, #12948, #13260, #12348, #18305 ) ) ;
#6885=EDGE_CURVE ( 'NONE', #1936, #4361, #5251, .T. ) ;
#6957=ORIENTED_EDGE ( 'NONE', *, *, #11417, .T. ) ;
#6987=ORIENTED_EDGE ( 'NONE', *, *, #1975, .T. ) ;
#6996=PLANE ( 'NONE',  #12425 ) ;
#7008=AXIS2_PLACEMENT_3D ( 'NONE', #8617, #2860, #11588 ) ;
#7019=CARTESIAN_POINT ( 'NONE',  ( 2.426025403784448642, 2.168404344971008868E-16, 0.000000000000000000 ) ) ;
#7020=EDGE_CURVE ( 'NONE', #17016, #6836, #12881, .T. ) ;
#7026=ORIENTED_EDGE ( 'NONE', *, *, #13916, .F. ) ;
#7065=VECTOR ( 'NONE', #18635, 1000.000000000000000 ) ;
#7103=DIRECTION ( 'NONE',  ( 0.000000000000000000, 0.000000000000000000, 1.000000000000000000 ) ) ;
#7141=ORIENTED_EDGE ( 'NONE', *, *, #2353, .F. ) ;
#7154=DIRECTION ( 'NONE',  ( 1.000000000000000000, 0.000000000000000000, 0.000000000000000000 ) ) ;
#7177=CARTESIAN_POINT ( 'NONE',  ( 2.369999999999999662, 0.000000000000000000, 0.000000000000000000 ) ) ;
#7182=CARTESIAN_POINT ( 'NONE',  ( 2.750000000000000000, 3.306546357697853240E-16, -2.699999999999999734 ) ) ;
#7206=AXIS2_PLACEMENT_3D ( 'NONE', #16877, #3781, #9610 ) ;
#7246=AXIS2_PLACEMENT_3D ( 'NONE', #18856, #29, #7601 ) ;
#7306=DIRECTION ( 'NONE',  ( -1.000000000000000000, 0.000000000000000000, 0.000000000000000000 ) ) ;
#7345=CARTESIAN_POINT ( 'NONE',  ( 1.560000000000000053, 0.000000000000000000, 2.999999999999998668 ) ) ;
#7357=ORIENTED_EDGE ( 'NONE', *, *, #8965, .F. ) ;
#7511=UNCERTAINTY_MEASURE_WITH_UNIT (LENGTH_MEASURE( 1.000000000000000082E-05 ), #607, 'distance_accuracy_value', 'NONE');
#7512=VECTOR ( 'NONE', #14192, 1000.000000000000114 ) ;
#7541=DIRECTION ( 'NONE',  ( 0.000000000000000000, 0.000000000000000000, 1.000000000000000000 ) ) ;
#7560=SPHERICAL_SURFACE ( 'NONE', #3819, 5.315148208181397216 ) ;
#7583=ORIENTED_EDGE ( 'NONE', *, *, #11417, .F. ) ;
#7590=DIRECTION ( 'NONE',  ( 0.000000000000000000, 0.000000000000000000, 1.000000000000000000 ) ) ;
#7592=AXIS2_PLACEMENT_3D ( 'NONE', #6147, #5152, #17810 ) ;
#7601=DIRECTION ( 'NONE',  ( 0.000000000000000000, 0.000000000000000000, 1.000000000000000000 ) ) ;
#7605=DIRECTION ( 'NONE',  ( -1.000000000000000000, 0.000000000000000000, 0.000000000000000000 ) ) ;
#7608=ORIENTED_EDGE ( 'NONE', *, *, #16394, .T. ) ;
#7644=DIRECTION ( 'NONE',  ( -0.000000000000000000, 0.000000000000000000, 1.000000000000000000 ) ) ;
#7679=CARTESIAN_POINT ( 'NONE',  ( 1.560000000000000053, 0.000000000000000000, 0.000000000000000000 ) ) ;
#7682=DIRECTION ( 'NONE',  ( -1.000000000000000000, -0.000000000000000000, -0.000000000000000000 ) ) ;
#7689=DIRECTION ( 'NONE',  ( -1.000000000000000000, -0.000000000000000000, -0.000000000000000000 ) ) ;
#7722=VERTEX_POINT ( 'NONE', #13173 ) ;
#7732=CYLINDRICAL_SURFACE ( 'NONE', #15424, 4.750000000000000000 ) ;
#7738=EDGE_LOOP ( 'NONE', ( #327, #12577, #3137, #9674, #18841 ) ) ;
#7739=ORIENTED_EDGE ( 'NONE', *, *, #16194, .T. ) ;
#7742=DIRECTION ( 'NONE',  ( 0.000000000000000000, 1.224646799147353207E-16, -1.000000000000000000 ) ) ;
#7749=CARTESIAN_POINT ( 'NONE',  ( 4.755015822784811164, -4.336808689942017736E-16, 0.000000000000000000 ) ) ;
#7766=VERTEX_POINT ( 'NONE', #3524 ) ;
#7829=EDGE_CURVE ( 'NONE', #18169, #2733, #9452, .T. ) ;
#7856=ADVANCED_FACE ( 'NONE', ( #2188 ), #3324, .T. ) ;
#7930=ADVANCED_FACE ( 'NONE', ( #9721 ), #844, .T. ) ;
#7942=AXIS2_PLACEMENT_3D ( 'NONE', #13060, #4756, #12017 ) ;
#7954=ADVANCED_FACE ( 'NONE', ( #12679 ), #16988, .T. ) ;
#7964=ORIENTED_EDGE ( 'NONE', *, *, #15446, .F. ) ;
#7970=SURFACE_SIDE_STYLE ('',( #16747 ) ) ;
#7972=FACE_OUTER_BOUND ( 'NONE', #10721, .T. ) ;
#8024=CARTESIAN_POINT ( 'NONE',  ( 2.949999999999999734, 0.000000000000000000, 2.499999999999999556 ) ) ;
#8047=AXIS2_PLACEMENT_3D ( 'NONE', #1461, #1360, #7103 ) ;
#8056=FACE_OUTER_BOUND ( 'NONE', #3594, .T. ) ;
#8078=DIRECTION ( 'NONE',  ( -0.000000000000000000, 1.000000000000000000, -0.000000000000000000 ) ) ;
#8091=ORIENTED_EDGE ( 'NONE', *, *, #9260, .T. ) ;
#8119=CARTESIAN_POINT ( 'NONE',  ( 0.000000000000000000, 0.000000000000000000, 0.000000000000000000 ) ) ;
#8130=CARTESIAN_POINT ( 'NONE',  ( 2.750000000000000000, 5.817072295949927426E-16, -4.750000000000000000 ) ) ;
#8147=FACE_OUTER_BOUND ( 'NONE', #4222, .T. ) ;
#8154=ORIENTED_EDGE ( 'NONE', *, *, #567, .F. ) ;
#8166=CIRCLE ( 'NONE', #9969, 2.499999999999999556 ) ;
#8182=ORIENTED_EDGE ( 'NONE', *, *, #1790, .F. ) ;
#8244=DIRECTION ( 'NONE',  ( 0.000000000000000000, -1.000000000000000000, 0.000000000000000000 ) ) ;
#8255=CARTESIAN_POINT ( 'NONE',  ( 2.949999999999999734, 0.000000000000000000, 0.000000000000000000 ) ) ;
#8284=AXIS2_PLACEMENT_3D ( 'NONE', #12691, #18521, #11275 ) ;
#8286=CARTESIAN_POINT ( 'NONE',  ( 18.75000000000000000, 0.000000000000000000, 2.055000000000000160 ) ) ;
#8290=ADVANCED_FACE ( 'NONE', ( #8972 ), #7560, .T. ) ;
#8335=DIRECTION ( 'NONE',  ( -1.000000000000000000, 0.000000000000000000, 0.000000000000000000 ) ) ;
#8377=VERTEX_POINT ( 'NONE', #665 ) ;
#8384=SURFACE_STYLE_FILL_AREA ( #16895 ) ;
#8413=VECTOR ( 'NONE', #6502, 999.9999999999998863 ) ;
#8451=EDGE_LOOP ( 'NONE', ( #10961, #11260, #2702, #1269, #10386 ) ) ;
#8453=DIRECTION ( 'NONE',  ( -1.000000000000000000, -0.000000000000000000, -0.000000000000000000 ) ) ;
#8462=LINE ( 'NONE', #17063, #7512 ) ;
#8465=PLANE ( 'NONE',  #10151 ) ;
#8525=FACE_OUTER_BOUND ( 'NONE', #12309, .T. ) ;
#8578=PLANE ( 'NONE',  #8284 ) ;
#8590=EDGE_CURVE ( 'NONE', #13735, #12765, #17555, .T. ) ;
#8617=CARTESIAN_POINT ( 'NONE',  ( 18.75000000000000000, 0.000000000000000000, 0.000000000000000000 ) ) ;
#8683=AXIS2_PLACEMENT_3D ( 'NONE', #8119, #13928, #4959 ) ;
#8706=ORIENTED_EDGE ( 'NONE', *, *, #12548, .F. ) ;
#8739=( GEOMETRIC_REPRESENTATION_CONTEXT ( 3 ) GLOBAL_UNCERTAINTY_ASSIGNED_CONTEXT ( ( #7511 ) ) GLOBAL_UNIT_ASSIGNED_CONTEXT ( ( #607, #9105, #6344 ) ) REPRESENTATION_CONTEXT ( 'NONE', 'WORKASPACE' ) );
#8760=EDGE_CURVE ( 'NONE', #6081, #13735, #12210, .T. ) ;
#8768=CIRCLE ( 'NONE', #10929, 5.315148208181397216 ) ;
#8774=CARTESIAN_POINT ( 'NONE',  ( 0.000000000000000000, 0.000000000000000000, 0.000000000000000000 ) ) ;
#8830=CIRCLE ( 'NONE', #6405, 1.500000000000000000 ) ;
#8844=DIRECTION ( 'NONE',  ( -1.000000000000000000, -0.000000000000000000, -0.000000000000000000 ) ) ;
#8888=CARTESIAN_POINT ( 'NONE',  ( 1.560000000000000053, 0.8660254037844389297, 1.500000000000000000 ) ) ;
#8891=DIRECTION ( 'NONE',  ( -1.000000000000000000, -0.000000000000000000, -0.000000000000000000 ) ) ;
#8896=ORIENTED_EDGE ( 'NONE', *, *, #16392, .T. ) ;
#8916=LINE ( 'NONE', #2698, #17184 ) ;
#8947=CARTESIAN_POINT ( 'NONE',  ( 1.560000000000000053, -0.8660254037844384856, 1.500000000000000000 ) ) ;
#8965=EDGE_CURVE ( 'NONE', #11688, #6836, #10074, .T. ) ;
#8972=FACE_OUTER_BOUND ( 'NONE', #12206, .T. ) ;
#9056=DIRECTION ( 'NONE',  ( -1.000000000000000000, -0.000000000000000000, -0.000000000000000000 ) ) ;
#9105=( NAMED_UNIT ( * ) PLANE_ANGLE_UNIT ( ) SI_UNIT ( $, .RADIAN. ) );
#9109=DIRECTION ( 'NONE',  ( -0.000000000000000000, 0.000000000000000000, 1.000000000000000000 ) ) ;
#9158=ORIENTED_EDGE ( 'NONE', *, *, #3114, .T. ) ;
#9187=ADVANCED_FACE ( 'NONE', ( #3852 ), #18291, .T. ) ;
#9260=EDGE_CURVE ( 'NONE', #15610, #11688, #10852, .T. ) ;
#9290=PRODUCT_DEFINITION_FORMATION_WITH_SPECIFIED_SOURCE ( 'ANY', '', #4477, .NOT_KNOWN. ) ;
#9327=AXIS2_PLACEMENT_3D ( 'NONE', #3896, #11076, #18506 ) ;
#9368=CARTESIAN_POINT ( 'NONE',  ( 0.000000000000000000, 2.375000000000000444, 0.000000000000000000 ) ) ;
#9393=LINE ( 'NONE', #15223, #17757 ) ;
#9406=ADVANCED_FACE ( 'NONE', ( #5550 ), #15711, .T. ) ;
#9426=ORIENTED_EDGE ( 'NONE', *, *, #13120, .T. ) ;
#9450=DIRECTION ( 'NONE',  ( 0.000000000000000000, 1.000000000000000000, 1.224646799147353454E-16 ) ) ;
#9452=LINE ( 'NONE', #13836, #12361 ) ;
#9505=ADVANCED_FACE ( 'NONE', ( #8147 ), #16745, .T. ) ;
#9507=DIRECTION ( 'NONE',  ( 0.000000000000000000, 0.000000000000000000, 1.000000000000000000 ) ) ;
#9508=AXIS2_PLACEMENT_3D ( 'NONE', #1849, #7689, #15306 ) ;
#9539=ORIENTED_EDGE ( 'NONE', *, *, #12186, .T. ) ;
#9540=CARTESIAN_POINT ( 'NONE',  ( 1.560000000000000053, -1.299038105676658450, 0.7500000000000007772 ) ) ;
#9555=CIRCLE ( 'NONE', #16276, 1.500000000000000000 ) ;
#9576=EDGE_CURVE ( 'NONE', #15271, #10362, #6430, .T. ) ;
#9610=DIRECTION ( 'NONE',  ( -0.000000000000000000, 0.000000000000000000, 1.000000000000000000 ) ) ;
#9611=CIRCLE ( 'NONE', #4426, 1.500000000000000000 ) ;
#9623=AXIS2_PLACEMENT_3D ( 'NONE', #1990, #18130, #16524 ) ;
#9646=ADVANCED_FACE ( 'NONE', ( #8056 ), #12256, .T. ) ;
#9674=ORIENTED_EDGE ( 'NONE', *, *, #11432, .F. ) ;
#9683=CARTESIAN_POINT ( 'NONE',  ( 1.560000000000000053, 0.000000000000000000, 2.999999999999998668 ) ) ;
#9721=FACE_OUTER_BOUND ( 'NONE', #14021, .T. ) ;
#9723=SURFACE_STYLE_USAGE ( .BOTH. , #12773 ) ;
#9749=CARTESIAN_POINT ( 'NONE',  ( 0.000000000000000000, -1.732050807568877859, -1.752539433813135784E-17 ) ) ;
#9770=CARTESIAN_POINT ( 'NONE',  ( 0.000000000000000000, 0.8660254037844389297, -1.500000000000000000 ) ) ;
#9795=EDGE_LOOP ( 'NONE', ( #11578, #5454, #7608, #2098, #4251 ) ) ;
#9796=EDGE_CURVE ( 'NONE', #7766, #18684, #3925, .T. ) ;
#9799=CARTESIAN_POINT ( 'NONE',  ( 1.560000000000000053, -1.732050807568877859, -1.752539433813135784E-17 ) ) ;
#9914=ORIENTED_EDGE ( 'NONE', *, *, #12637, .T. ) ;
#9928=DIRECTION ( 'NONE',  ( -0.000000000000000000, 1.000000000000000000, 1.224646799147353207E-16 ) ) ;
#9953=DIRECTION ( 'NONE',  ( 0.000000000000000000, 0.000000000000000000, 1.000000000000000000 ) ) ;
#9969=AXIS2_PLACEMENT_3D ( 'NONE', #6373, #6653, #9507 ) ;
#9970=VECTOR ( 'NONE', #12650, 1000.000000000000000 ) ;
#9985=EDGE_CURVE ( 'NONE', #3140, #18169, #8462, .T. ) ;
#10016=DIRECTION ( 'NONE',  ( -1.000000000000000000, -0.000000000000000000, -0.000000000000000000 ) ) ;
#10025=CARTESIAN_POINT ( 'NONE',  ( 2.369999999999999662, -4.750000000000000888, -5.817072295949926440E-16 ) ) ;
#10026=ADVANCED_FACE ( 'NONE', ( #11060, #6666 ), #12479, .F. ) ;
#10035=CARTESIAN_POINT ( 'NONE',  ( 0.000000000000000000, 0.8660254037844389297, 1.500000000000000000 ) ) ;
#10070=EDGE_LOOP ( 'NONE', ( #1101, #17454 ) ) ;
#10074=LINE ( 'NONE', #5762, #16678 ) ;
#10138=CARTESIAN_POINT ( 'NONE',  ( 0.000000000000000000, 0.000000000000000000, 4.750000000000000000 ) ) ;
#10151=AXIS2_PLACEMENT_3D ( 'NONE', #4165, #2798, #17738 ) ;
#10170=DIRECTION ( 'NONE',  ( -0.000000000000000000, 0.5000000000000004441, 0.8660254037844383745 ) ) ;
#10195=FACE_OUTER_BOUND ( 'NONE', #9795, .T. ) ;
#10257=VERTEX_POINT ( 'NONE', #4733 ) ;
#10262=DIRECTION ( 'NONE',  ( -0.000000000000000000, 1.000000000000000000, -0.000000000000000000 ) ) ;
#10278=VECTOR ( 'NONE', #7306, 1000.000000000000000 ) ;
#10296=EDGE_CURVE ( 'NONE', #7722, #6395, #11995, .T. ) ;
#10300=LINE ( 'NONE', #13253, #4751 ) ;
#10362=VERTEX_POINT ( 'NONE', #17692 ) ;
#10373=CARTESIAN_POINT ( 'NONE',  ( 2.750000000000000000, 0.000000000000000000, 0.000000000000000000 ) ) ;
#10378=ORIENTED_EDGE ( 'NONE', *, *, #4634, .T. ) ;
#10385=CARTESIAN_POINT ( 'NONE',  ( 1.560000000000000053, 1.732050807568878747, 7.017607234860990640E-28 ) ) ;
#10386=ORIENTED_EDGE ( 'NONE', *, *, #15735, .F. ) ;
#10395=FACE_BOUND ( 'NONE', #6131, .T. ) ;
#10421=DIRECTION ( 'NONE',  ( 0.000000000000000000, 0.000000000000000000, -1.000000000000000000 ) ) ;
#10453=PLANE ( 'NONE',  #261 ) ;
#10458=EDGE_LOOP ( 'NONE', ( #9539, #13142 ) ) ;
#10487=CARTESIAN_POINT ( 'NONE',  ( -997.5739745962155212, 0.000000000000000000, 0.000000000000000000 ) ) ;
#10489=CIRCLE ( 'NONE', #12919, 4.750000000000000000 ) ;
#10510=ORIENTED_EDGE ( 'NONE', *, *, #2679, .T. ) ;
#10581=MECHANICAL_DESIGN_GEOMETRIC_PRESENTATION_REPRESENTATION('',(#18214),#8739);
#10595=CARTESIAN_POINT ( 'NONE',  ( 0.000000000000000000, 0.000000000000000000, 0.000000000000000000 ) ) ;
#10609=STYLED_ITEM ( 'NONE', ( #3799 ), #16636 ) ;
#10689=LINE ( 'NONE', #1988, #661 ) ;
#10721=EDGE_LOOP ( 'NONE', ( #16750, #8091, #2376, #14962, #1418 ) ) ;
#10725=DIRECTION ( 'NONE',  ( -1.000000000000000000, 0.000000000000000000, 0.000000000000000000 ) ) ;
#10732=SURFACE_STYLE_USAGE ( .BOTH. , #7970 ) ;
#10771=ORIENTED_EDGE ( 'NONE', *, *, #13916, .T. ) ;
#10776=PRODUCT_DEFINITION_CONTEXT ( 'detailed design', #5684, 'design' ) ;
#10813=AXIS2_PLACEMENT_3D ( 'NONE', #2910, #13059, #4082 ) ;
#10852=LINE ( 'NONE', #2233, #13278 ) ;
#10929=AXIS2_PLACEMENT_3D ( 'NONE', #13784, #2138, #15131 ) ;
#10946=EDGE_CURVE ( 'NONE', #18169, #2106, #9555, .T. ) ;
#10959=CARTESIAN_POINT ( 'NONE',  ( 2.750000000000000000, 0.000000000000000000, 4.750000000000000000 ) ) ;
#10961=ORIENTED_EDGE ( 'NONE', *, *, #12217, .T. ) ;
#10986=DIRECTION ( 'NONE',  ( -0.000000000000000000, 0.5000000000000003331, -0.8660254037844384856 ) ) ;
#10990=ORIENTED_EDGE ( 'NONE', *, *, #10296, .T. ) ;
#11019=ADVANCED_FACE ( 'NONE', ( #2617 ), #8465, .T. ) ;
#11060=FACE_BOUND ( 'NONE', #10458, .T. ) ;
#11076=DIRECTION ( 'NONE',  ( 0.000000000000000000, -0.8660254037844384856, 0.5000000000000004441 ) ) ;
#11127=AXIS2_PLACEMENT_3D ( 'NONE', #4754, #5990, #4851 ) ;
#11209=CARTESIAN_POINT ( 'NONE',  ( 1.560000000000000053, 0.8660254037844389297, 1.500000000000000000 ) ) ;
#11225=COLOUR_RGB ( '', 0.72549020, 0.75294118, 0.79215686) ;
#11248=DIRECTION ( 'NONE',  ( 0.000000000000000000, 0.000000000000000000, 1.000000000000000000 ) ) ;
#11260=ORIENTED_EDGE ( 'NONE', *, *, #6533, .T. ) ;
#11271=LINE ( 'NONE', #18516, #12723 ) ;
#11275=DIRECTION ( 'NONE',  ( 0.000000000000000000, 0.000000000000000000, 1.000000000000000000 ) ) ;
#11324=VERTEX_POINT ( 'NONE', #9770 ) ;
#11337=DIRECTION ( 'NONE',  ( -1.000000000000000000, -0.000000000000000000, -0.000000000000000000 ) ) ;
#11346=ORIENTED_EDGE ( 'NONE', *, *, #3865, .T. ) ;
#11347=FACE_OUTER_BOUND ( 'NONE', #18235, .T. ) ;
#11417=EDGE_CURVE ( 'NONE', #3140, #18684, #1552, .T. ) ;
#11429=AXIS2_PLACEMENT_3D ( 'NONE', #14644, #11977, #9109 ) ;
#11432=EDGE_CURVE ( 'NONE', #1936, #7722, #5569, .T. ) ;
#11438=ORIENTED_EDGE ( 'NONE', *, *, #1098, .F. ) ;
#11454=AXIS2_PLACEMENT_3D ( 'NONE', #13588, #2303, #15121 ) ;
#11578=ORIENTED_EDGE ( 'NONE', *, *, #9576, .F. ) ;
#11588=DIRECTION ( 'NONE',  ( 0.000000000000000000, 0.000000000000000000, 1.000000000000000000 ) ) ;
#11589=CARTESIAN_POINT ( 'NONE',  ( 2.949999999999999734, 0.000000000000000000, 0.000000000000000000 ) ) ;
#11626=FACE_OUTER_BOUND ( 'NONE', #8451, .T. ) ;
#11640=EDGE_CURVE ( 'NONE', #17865, #1087, #18416, .T. ) ;
#11647=AXIS2_PLACEMENT_3D ( 'NONE', #609, #12260, #18090 ) ;
#11688=VERTEX_POINT ( 'NONE', #5533 ) ;
#11776=CARTESIAN_POINT ( 'NONE',  ( -997.5739745962155212, 0.000000000000000000, 0.000000000000000000 ) ) ;
#11803=CARTESIAN_POINT ( 'NONE',  ( 2.750000000000000000, 0.000000000000000000, 2.699999999999999734 ) ) ;
#11815=VERTEX_POINT ( 'NONE', #7182 ) ;
#11826=VECTOR ( 'NONE', #1626, 1000.000000000000000 ) ;
#11828=PLANE ( 'NONE',  #3947 ) ;
#11886=VERTEX_POINT ( 'NONE', #3036 ) ;
#11920=DIRECTION ( 'NONE',  ( 0.000000000000000000, 0.000000000000000000, 1.000000000000000000 ) ) ;
#11964=ORIENTED_EDGE ( 'NONE', *, *, #7829, .T. ) ;
#11977=DIRECTION ( 'NONE',  ( -1.000000000000000000, 0.000000000000000000, -0.000000000000000000 ) ) ;
#11995=CIRCLE ( 'NONE', #5270, 4.750000000000000000 ) ;
#12017=DIRECTION ( 'NONE',  ( 0.000000000000000000, 0.000000000000000000, 1.000000000000000000 ) ) ;
#12022=AXIS2_PLACEMENT_3D ( 'NONE', #5414, #17079, #2531 ) ;
#12037=DIRECTION ( 'NONE',  ( -1.000000000000000000, -0.000000000000000000, -0.000000000000000000 ) ) ;
#12041=VERTEX_POINT ( 'NONE', #8286 ) ;
#12136=VECTOR ( 'NONE', #16004, 1000.000000000000114 ) ;
#12186=EDGE_CURVE ( 'NONE', #17865, #11815, #1943, .T. ) ;
#12206=EDGE_LOOP ( 'NONE', ( #14600, #14822, #16135, #11438, #7964 ) ) ;
#12210=LINE ( 'NONE', #10385, #16969 ) ;
#12217=EDGE_CURVE ( 'NONE', #5916, #13259, #10489, .T. ) ;
#12244=ORIENTED_EDGE ( 'NONE', *, *, #18401, .F. ) ;
#12256=PLANE ( 'NONE',  #17883 ) ;
#12260=DIRECTION ( 'NONE',  ( 0.000000000000000000, 0.000000000000000000, 1.000000000000000000 ) ) ;
#12309=EDGE_LOOP ( 'NONE', ( #3418, #2180, #11346, #1761, #14622 ) ) ;
#12341=CARTESIAN_POINT ( 'NONE',  ( 2.426025403784448642, 0.000000000000000000, 2.168404344971008868E-16 ) ) ;
#12348=ORIENTED_EDGE ( 'NONE', *, *, #3114, .F. ) ;
#12361=VECTOR ( 'NONE', #10986, 1000.000000000000114 ) ;
#12366=CARTESIAN_POINT ( 'NONE',  ( 18.75000000000000000, 0.000000000000000000, 2.055000000000000160 ) ) ;
#12379=LINE ( 'NONE', #18209, #9970 ) ;
#12404=CARTESIAN_POINT ( 'NONE',  ( 18.30499999999999972, 0.000000000000000000, 2.499999999999999556 ) ) ;
#12425=AXIS2_PLACEMENT_3D ( 'NONE', #18830, #8335, #15581 ) ;
#12479=PLANE ( 'NONE',  #7206 ) ;
#12547=LINE ( 'NONE', #12366, #2342 ) ;
#12548=EDGE_CURVE ( 'NONE', #13259, #5916, #2771, .T. ) ;
#12561=ADVANCED_FACE ( 'NONE', ( #7972 ), #13696, .T. ) ;
#12569=EDGE_CURVE ( 'NONE', #3637, #11886, #9393, .T. ) ;
#12570=DIRECTION ( 'NONE',  ( 0.000000000000000000, 0.000000000000000000, 1.000000000000000000 ) ) ;
#12577=ORIENTED_EDGE ( 'NONE', *, *, #12548, .T. ) ;
#12584=FILL_AREA_STYLE_COLOUR ( '', #11225 ) ;
#12637=EDGE_CURVE ( 'NONE', #17016, #5495, #17113, .T. ) ;
#12650=DIRECTION ( 'NONE',  ( -0.000000000000000000, 1.000000000000000000, -0.000000000000000000 ) ) ;
#12679=FACE_OUTER_BOUND ( 'NONE', #6883, .T. ) ;
#12682=( NAMED_UNIT ( * ) PLANE_ANGLE_UNIT ( ) SI_UNIT ( $, .RADIAN. ) );
#12691=CARTESIAN_POINT ( 'NONE',  ( 1.560000000000000053, 0.000000000000000000, 2.999999999999998668 ) ) ;
#12704=COLOUR_RGB ( '', 0.72549020, 0.75294118, 0.79215686) ;
#12712=CARTESIAN_POINT ( 'NONE',  ( 1.560000000000000053, -1.299038105676658450, -0.7500000000000007772 ) ) ;
#12723=VECTOR ( 'NONE', #13937, 1000.000000000000000 ) ;
#12748=ADVANCED_FACE ( 'NONE', ( #5821 ), #15868, .T. ) ;
#12756=PLANE ( 'NONE',  #5949 ) ;
#12765=VERTEX_POINT ( 'NONE', #10035 ) ;
#12773=SURFACE_SIDE_STYLE ('',( #8384 ) ) ;
#12789=CONICAL_SURFACE ( 'NONE', #7942, 2.055000000000000160, 0.7853981633974468357 ) ;
#12881=CIRCLE ( 'NONE', #16565, 1.500000000000000000 ) ;
#12892=LINE ( 'NONE', #13180, #14013 ) ;
#12904=DIRECTION ( 'NONE',  ( 0.000000000000000000, 1.000000000000000000, 0.000000000000000000 ) ) ;
#12919=AXIS2_PLACEMENT_3D ( 'NONE', #6372, #13521, #3585 ) ;
#12948=ORIENTED_EDGE ( 'NONE', *, *, #3109, .T. ) ;
#12960=AXIS2_PLACEMENT_3D ( 'NONE', #9799, #5322, #18686 ) ;
#12966=FACE_OUTER_BOUND ( 'NONE', #2003, .T. ) ;
#12973=ORIENTED_EDGE ( 'NONE', *, *, #5105, .F. ) ;
#12979=ADVANCED_FACE ( 'NONE', ( #10195 ), #15593, .F. ) ;
#13057=ORIENTED_EDGE ( 'NONE', *, *, #8590, .F. ) ;
#13059=DIRECTION ( 'NONE',  ( -1.000000000000000000, -0.000000000000000000, -0.000000000000000000 ) ) ;
#13060=CARTESIAN_POINT ( 'NONE',  ( 18.75000000000000000, 0.000000000000000000, 0.000000000000000000 ) ) ;
#13099=CIRCLE ( 'NONE', #7008, 2.055000000000000160 ) ;
#13120=EDGE_CURVE ( 'NONE', #2733, #10257, #10689, .T. ) ;
#13122=CARTESIAN_POINT ( 'NONE',  ( 1.560000000000000053, 1.732050807568878747, 7.017607234860990640E-28 ) ) ;
#13124=CARTESIAN_POINT ( 'NONE',  ( 1.560000000000000053, -0.8660254037844384856, 1.500000000000000000 ) ) ;
#13142=ORIENTED_EDGE ( 'NONE', *, *, #951, .T. ) ;
#13173=CARTESIAN_POINT ( 'NONE',  ( 2.369999999999999662, 0.000000000000000000, 4.750000000000000000 ) ) ;
#13180=CARTESIAN_POINT ( 'NONE',  ( 2.426025403784448642, 2.655529440325959183E-32, -2.168404344971008868E-16 ) ) ;
#13205=( NAMED_UNIT ( * ) PLANE_ANGLE_UNIT ( ) SI_UNIT ( $, .RADIAN. ) );
#13214=EDGE_LOOP ( 'NONE', ( #7141, #13579, #15918 ) ) ;
#13216=ORIENTED_EDGE ( 'NONE', *, *, #15004, .F. ) ;
#13220=AXIS2_PLACEMENT_3D ( 'NONE', #10373, #8844, #16203 ) ;
#13229=DIRECTION ( 'NONE',  ( 0.000000000000000000, -0.8660254037844384856, -0.5000000000000004441 ) ) ;
#13253=CARTESIAN_POINT ( 'NONE',  ( 0.000000000000000000, -0.8660254037844384856, 1.500000000000000000 ) ) ;
#13259=VERTEX_POINT ( 'NONE', #8130 ) ;
#13260=ORIENTED_EDGE ( 'NONE', *, *, #8760, .T. ) ;
#13278=VECTOR ( 'NONE', #8078, 1000.000000000000000 ) ;
#13303=CARTESIAN_POINT ( 'NONE',  ( 1.560000000000000053, -1.732050807568877859, -1.752539433813135784E-17 ) ) ;
#13350=DIRECTION ( 'NONE',  ( -0.000000000000000000, -1.000000000000000000, -0.000000000000000000 ) ) ;
#13375=CIRCLE ( 'NONE', #7592, 4.750000000000000000 ) ;
#13388=ADVANCED_FACE ( 'NONE', ( #12966 ), #8578, .T. ) ;
#13422=CARTESIAN_POINT ( 'NONE',  ( 1.560000000000000053, 0.000000000000000000, 0.000000000000000000 ) ) ;
#13506=ADVANCED_FACE ( 'NONE', ( #17564, #10395 ), #4473, .T. ) ;
#13521=DIRECTION ( 'NONE',  ( -1.000000000000000000, -0.000000000000000000, -0.000000000000000000 ) ) ;
#13530=ORIENTED_EDGE ( 'NONE', *, *, #16833, .T. ) ;
#13542=CARTESIAN_POINT ( 'NONE',  ( 0.000000000000000000, -1.732050807568877859, -1.752539433813135784E-17 ) ) ;
#13579=ORIENTED_EDGE ( 'NONE', *, *, #12637, .F. ) ;
#13588=CARTESIAN_POINT ( 'NONE',  ( 1.560000000000000053, -0.8660254037844384856, -1.500000000000000000 ) ) ;
#13599=VECTOR ( 'NONE', #5620, 1000.000000000000114 ) ;
#13600=ORIENTED_EDGE ( 'NONE', *, *, #6801, .T. ) ;
#13696=PLANE ( 'NONE',  #11647 ) ;
#13735=VERTEX_POINT ( 'NONE', #14099 ) ;
#13737=FACE_OUTER_BOUND ( 'NONE', #5894, .T. ) ;
#13743=ORIENTED_EDGE ( 'NONE', *, *, #9796, .F. ) ;
#13779=SHAPE_REPRESENTATION_RELATIONSHIP ( 'NONE' , 'NONE' ,  #4478, #18307 ) ;
#13784=CARTESIAN_POINT ( 'NONE',  ( 4.755015822784811164, -4.336808689942017736E-16, 0.000000000000000000 ) ) ;
#13836=CARTESIAN_POINT ( 'NONE',  ( 1.560000000000000053, -0.8660254037844384856, -1.500000000000000000 ) ) ;
#13842=CARTESIAN_POINT ( 'NONE',  ( 0.000000000000000000, -2.375000000000000444, -4.362804221962445569E-16 ) ) ;
#13857=DIRECTION ( 'NONE',  ( 0.000000000000000000, 0.000000000000000000, 1.000000000000000000 ) ) ;
#13916=EDGE_CURVE ( 'NONE', #6081, #17016, #47, .T. ) ;
#13928=DIRECTION ( 'NONE',  ( -1.000000000000000000, -0.000000000000000000, -0.000000000000000000 ) ) ;
#13937=DIRECTION ( 'NONE',  ( -0.000000000000000000, 0.5000000000000004441, 0.8660254037844383745 ) ) ;
#13971=VECTOR ( 'NONE', #5867, 1000.000000000000000 ) ;
#14013=VECTOR ( 'NONE', #4300, 1000.000000000000114 ) ;
#14021=EDGE_LOOP ( 'NONE', ( #17988, #14185, #6957, #13743, #18391 ) ) ;
#14099=CARTESIAN_POINT ( 'NONE',  ( 0.000000000000000000, 1.732050807568878747, 7.017607234860990640E-28 ) ) ;
#14148=CIRCLE ( 'NONE', #10813, 1.500000000000000000 ) ;
#14156=ORIENTED_EDGE ( 'NONE', *, *, #11640, .T. ) ;
#14184=ORIENTED_EDGE ( 'NONE', *, *, #2679, .F. ) ;
#14185=ORIENTED_EDGE ( 'NONE', *, *, #15004, .T. ) ;
#14192=DIRECTION ( 'NONE',  ( -0.000000000000000000, 0.5000000000000003331, -0.8660254037844384856 ) ) ;
#14211=DIRECTION ( 'NONE',  ( -1.000000000000000000, -0.000000000000000000, -0.000000000000000000 ) ) ;
#14248=AXIS2_PLACEMENT_3D ( 'NONE', #5248, #15561, #2378 ) ;
#14257=VECTOR ( 'NONE', #10725, 1000.000000000000000 ) ;
#14263=ORIENTED_EDGE ( 'NONE', *, *, #15156, .F. ) ;
#14354=CARTESIAN_POINT ( 'NONE',  ( 1.560000000000000053, -0.8660254037844384856, 1.500000000000000000 ) ) ;
#14408=EDGE_CURVE ( 'NONE', #6395, #17499, #13375, .T. ) ;
#14468=EDGE_CURVE ( 'NONE', #1087, #11886, #6048, .T. ) ;
#14552=VECTOR ( 'NONE', #4333, 1000.000000000000000 ) ;
#14556=ORIENTED_EDGE ( 'NONE', *, *, #680, .T. ) ;
#14579=ORIENTED_EDGE ( 'NONE', *, *, #7020, .F. ) ;
#14600=ORIENTED_EDGE ( 'NONE', *, *, #14408, .T. ) ;
#14622=ORIENTED_EDGE ( 'NONE', *, *, #4417, .T. ) ;
#14636=ORIENTED_EDGE ( 'NONE', *, *, #5521, .F. ) ;
#14644=CARTESIAN_POINT ( 'NONE',  ( 18.75000000000000000, 0.000000000000000000, 0.000000000000000000 ) ) ;
#14678=DIRECTION ( 'NONE',  ( -0.000000000000000000, -0.5000000000000004441, 0.8660254037844383745 ) ) ;
#14696=DIRECTION ( 'NONE',  ( 0.000000000000000000, 0.000000000000000000, 1.000000000000000000 ) ) ;
#14698=CARTESIAN_POINT ( 'NONE',  ( 2.750000000000000000, 0.000000000000000000, 0.000000000000000000 ) ) ;
#14754=UNCERTAINTY_MEASURE_WITH_UNIT (LENGTH_MEASURE( 1.000000000000000082E-05 ), #15885, 'distance_accuracy_value', 'NONE');
#14822=ORIENTED_EDGE ( 'NONE', *, *, #5747, .T. ) ;
#14867=( GEOMETRIC_REPRESENTATION_CONTEXT ( 3 ) GLOBAL_UNCERTAINTY_ASSIGNED_CONTEXT ( ( #17044 ) ) GLOBAL_UNIT_ASSIGNED_CONTEXT ( ( #2448, #12682, #17168 ) ) REPRESENTATION_CONTEXT ( 'NONE', 'WORKASPACE' ) );
#14922=DIRECTION ( 'NONE',  ( 0.000000000000000000, 0.000000000000000000, 1.000000000000000000 ) ) ;
#14962=ORIENTED_EDGE ( 'NONE', *, *, #16194, .F. ) ;
#15004=EDGE_CURVE ( 'NONE', #2106, #3140, #4550, .T. ) ;
#15036=ORIENTED_EDGE ( 'NONE', *, *, #14468, .F. ) ;
#15092=DIRECTION ( 'NONE',  ( 0.000000000000000000, 0.000000000000000000, -1.000000000000000000 ) ) ;
#15106=ORIENTED_EDGE ( 'NONE', *, *, #12217, .F. ) ;
#15121=DIRECTION ( 'NONE',  ( 0.000000000000000000, -0.5000000000000003331, 0.8660254037844383745 ) ) ;
#15131=DIRECTION ( 'NONE',  ( 1.000000000000000000, 0.000000000000000000, 0.000000000000000000 ) ) ;
#15156=EDGE_CURVE ( 'NONE', #1137, #3637, #8166, .T. ) ;
#15174=CIRCLE ( 'NONE', #7246, 1.500000000000000000 ) ;
#15180=VECTOR ( 'NONE', #15638, 1000.000000000000000 ) ;
#15181=AXIS2_PLACEMENT_3D ( 'NONE', #11776, #4230, #4515 ) ;
#15223=CARTESIAN_POINT ( 'NONE',  ( 0.000000000000000000, 3.061616997868382648E-16, -2.499999999999999556 ) ) ;
#15238=DIRECTION ( 'NONE',  ( -0.7071067811865486830, 0.000000000000000000, 0.7071067811865464625 ) ) ;
#15271=VERTEX_POINT ( 'NONE', #7019 ) ;
#15293=AXIS2_PLACEMENT_3D ( 'NONE', #10595, #16330, #7644 ) ;
#15298=CARTESIAN_POINT ( 'NONE',  ( 1.560000000000000053, -1.732050807568877859, -1.752539433813135784E-17 ) ) ;
#15306=DIRECTION ( 'NONE',  ( 0.000000000000000000, 0.000000000000000000, 1.000000000000000000 ) ) ;
#15323=VECTOR ( 'NONE', #8891, 1000.000000000000000 ) ;
#15358=CARTESIAN_POINT ( 'NONE',  ( 1.560000000000000053, 0.000000000000000000, 0.000000000000000000 ) ) ;
#15424=AXIS2_PLACEMENT_3D ( 'NONE', #8774, #9056, #7541 ) ;
#15446=EDGE_CURVE ( 'NONE', #6395, #18405, #8768, .T. ) ;
#15561=DIRECTION ( 'NONE',  ( -1.000000000000000000, -0.000000000000000000, -0.000000000000000000 ) ) ;
#15581=DIRECTION ( 'NONE',  ( 0.000000000000000000, 0.000000000000000000, 1.000000000000000000 ) ) ;
#15593=CONICAL_SURFACE ( 'NONE', #18055, 1732.050807568857181, 1.047197551196592746 ) ;
#15610=VERTEX_POINT ( 'NONE', #5538 ) ;
#15638=DIRECTION ( 'NONE',  ( -0.000000000000000000, 0.5000000000000004441, 0.8660254037844383745 ) ) ;
#15706=DIRECTION ( 'NONE',  ( 0.000000000000000000, 0.000000000000000000, 1.000000000000000000 ) ) ;
#15711=CONICAL_SURFACE ( 'NONE', #18175, 2.055000000000000160, 0.7853981633974468357 ) ;
#15716=CARTESIAN_POINT ( 'NONE',  ( 0.000000000000000000, 0.000000000000000000, 0.000000000000000000 ) ) ;
#15735=EDGE_CURVE ( 'NONE', #5916, #7722, #4313, .T. ) ;
#15748=ORIENTED_EDGE ( 'NONE', *, *, #14468, .T. ) ;
#15812=AXIS2_PLACEMENT_3D ( 'NONE', #8255, #3662, #6539 ) ;
#15847=CIRCLE ( 'NONE', #18299, 2.699999999999999734 ) ;
#15868=SPHERICAL_SURFACE ( 'NONE', #17445, 5.315148208181397216 ) ;
#15885=( LENGTH_UNIT ( ) NAMED_UNIT ( * ) SI_UNIT ( .MILLI., .METRE. ) );
#15918=ORIENTED_EDGE ( 'NONE', *, *, #3865, .F. ) ;
#15949=VECTOR ( 'NONE', #120, 1000.000000000000000 ) ;
#15992=ORIENTED_EDGE ( 'NONE', *, *, #1098, .T. ) ;
#16004=DIRECTION ( 'NONE',  ( -0.000000000000000000, -0.5000000000000003331, -0.8660254037844384856 ) ) ;
#16022=DIRECTION ( 'NONE',  ( -1.000000000000000000, -0.000000000000000000, -0.000000000000000000 ) ) ;
#16094=MECHANICAL_DESIGN_GEOMETRIC_PRESENTATION_REPRESENTATION('',(#10609),#14867);
#16097=EDGE_LOOP ( 'NONE', ( #3998, #3118, #13530, #14636 ) ) ;
#16112=CARTESIAN_POINT ( 'NONE',  ( 1.560000000000000053, -1.732050807568877859, -1.752539433813135784E-17 ) ) ;
#16124=ORIENTED_EDGE ( 'NONE', *, *, #7829, .F. ) ;
#16127=FACE_OUTER_BOUND ( 'NONE', #6064, .T. ) ;
#16135=ORIENTED_EDGE ( 'NONE', *, *, #6885, .T. ) ;
#16165=DIRECTION ( 'NONE',  ( -0.000000000000000000, 0.5000000000000003331, -0.8660254037844384856 ) ) ;
#16179=FACE_OUTER_BOUND ( 'NONE', #10070, .T. ) ;
#16191=ORIENTED_EDGE ( 'NONE', *, *, #10946, .F. ) ;
#16194=EDGE_CURVE ( 'NONE', #10257, #11324, #12379, .T. ) ;
#16203=DIRECTION ( 'NONE',  ( 0.000000000000000000, 0.000000000000000000, 1.000000000000000000 ) ) ;
#16217=DIRECTION ( 'NONE',  ( -1.000000000000000000, 0.000000000000000000, 0.000000000000000000 ) ) ;
#16219=LINE ( 'NONE', #8947, #4734 ) ;
#16235=ORIENTED_EDGE ( 'NONE', *, *, #18762, .F. ) ;
#16260=DIRECTION ( 'NONE',  ( -1.000000000000000000, -0.000000000000000000, -0.000000000000000000 ) ) ;
#16276=AXIS2_PLACEMENT_3D ( 'NONE', #18583, #11337, #12570 ) ;
#16295=AXIS2_PLACEMENT_3D ( 'NONE', #5499, #14211, #18504 ) ;
#16330=DIRECTION ( 'NONE',  ( -1.000000000000000000, 0.000000000000000000, -0.000000000000000000 ) ) ;
#16335=AXIS2_PLACEMENT_3D ( 'NONE', #17580, #9928, #4494 ) ;
#16363=LINE ( 'NONE', #17497, #15323 ) ;
#16378=( GEOMETRIC_REPRESENTATION_CONTEXT ( 3 ) GLOBAL_UNCERTAINTY_ASSIGNED_CONTEXT ( ( #14754 ) ) GLOBAL_UNIT_ASSIGNED_CONTEXT ( ( #15885, #13205, #694 ) ) REPRESENTATION_CONTEXT ( 'NONE', 'WORKASPACE' ) );
#16380=CARTESIAN_POINT ( 'NONE',  ( 1.560000000000000053, 0.8660254037844389297, 1.500000000000000000 ) ) ;
#16392=EDGE_CURVE ( 'NONE', #2855, #7766, #5750, .T. ) ;
#16394=EDGE_CURVE ( 'NONE', #15610, #18169, #15174, .T. ) ;
#16436=ORIENTED_EDGE ( 'NONE', *, *, #8965, .T. ) ;
#16524=DIRECTION ( 'NONE',  ( 0.000000000000000000, 0.000000000000000000, 1.000000000000000000 ) ) ;
#16533=ORIENTED_EDGE ( 'NONE', *, *, #8760, .F. ) ;
#16565=AXIS2_PLACEMENT_3D ( 'NONE', #15358, #8453, #15706 ) ;
#16576=FACE_OUTER_BOUND ( 'NONE', #1469, .T. ) ;
#16597=EDGE_LOOP ( 'NONE', ( #5091, #57, #10990, #16635, #2995 ) ) ;
#16614=ORIENTED_EDGE ( 'NONE', *, *, #6035, .F. ) ;
#16635=ORIENTED_EDGE ( 'NONE', *, *, #15446, .T. ) ;
#16636=MANIFOLD_SOLID_BREP ( 'Hex', #17940 ) ;
#16652=PRESENTATION_STYLE_ASSIGNMENT (( #10732 ) ) ;
#16678=VECTOR ( 'NONE', #10170, 1000.000000000000000 ) ;
#16691=ORIENTED_EDGE ( 'NONE', *, *, #567, .T. ) ;
#16745=PLANE ( 'NONE',  #11454 ) ;
#16747=SURFACE_STYLE_FILL_AREA ( #3358 ) ;
#16750=ORIENTED_EDGE ( 'NONE', *, *, #130, .T. ) ;
#16766=DIRECTION ( 'NONE',  ( 0.000000000000000000, 0.000000000000000000, 1.000000000000000000 ) ) ;
#16767=CARTESIAN_POINT ( 'NONE',  ( 1.560000000000000053, -0.8660254037844384856, -1.500000000000000000 ) ) ;
#16803=CIRCLE ( 'NONE', #6745, 2.499999999999999556 ) ;
#16833=EDGE_CURVE ( 'NONE', #11886, #1087, #16803, .T. ) ;
#16877=CARTESIAN_POINT ( 'NONE',  ( 2.750000000000000000, 2.499999999999999112, 0.000000000000000000 ) ) ;
#16895=FILL_AREA_STYLE ('',( #12584 ) ) ;
#16942=FACE_OUTER_BOUND ( 'NONE', #5040, .T. ) ;
#16969=VECTOR ( 'NONE', #16217, 1000.000000000000000 ) ;
#16988=PLANE ( 'NONE',  #9327 ) ;
#17016=VERTEX_POINT ( 'NONE', #507 ) ;
#17044=UNCERTAINTY_MEASURE_WITH_UNIT (LENGTH_MEASURE( 1.000000000000000082E-05 ), #2448, 'distance_accuracy_value', 'NONE');
#17056=ORIENTED_EDGE ( 'NONE', *, *, #9985, .T. ) ;
#17063=CARTESIAN_POINT ( 'NONE',  ( 1.560000000000000053, -0.8660254037844384856, -1.500000000000000000 ) ) ;
#17079=DIRECTION ( 'NONE',  ( -1.000000000000000000, -0.000000000000000000, -0.000000000000000000 ) ) ;
#17100=ORIENTED_EDGE ( 'NONE', *, *, #1975, .F. ) ;
#17112=CARTESIAN_POINT ( 'NONE',  ( 2.949999999999999734, 0.000000000000000000, 2.699999999999999734 ) ) ;
#17113=LINE ( 'NONE', #11209, #7065 ) ;
#17168=( NAMED_UNIT ( * ) SI_UNIT ( $, .STERADIAN. ) SOLID_ANGLE_UNIT ( ) );
#17184=VECTOR ( 'NONE', #10262, 1000.000000000000000 ) ;
#17249=DIRECTION ( 'NONE',  ( 1.000000000000000000, 0.000000000000000000, 0.000000000000000000 ) ) ;
#17436=ADVANCED_FACE ( 'NONE', ( #16127 ), #12789, .T. ) ;
#17439=ADVANCED_FACE ( 'NONE', ( #2912 ), #11828, .T. ) ;
#17445=AXIS2_PLACEMENT_3D ( 'NONE', #5726, #10421, #12904 ) ;
#17454=ORIENTED_EDGE ( 'NONE', *, *, #4634, .F. ) ;
#17497=CARTESIAN_POINT ( 'NONE',  ( 0.000000000000000000, 5.817072295949927426E-16, -4.750000000000000000 ) ) ;
#17499=VERTEX_POINT ( 'NONE', #17758 ) ;
#17555=LINE ( 'NONE', #18599, #2028 ) ;
#17564=FACE_OUTER_BOUND ( 'NONE', #6033, .T. ) ;
#17575=DIRECTION ( 'NONE',  ( -1.000000000000000000, -0.000000000000000000, -0.000000000000000000 ) ) ;
#17580=CARTESIAN_POINT ( 'NONE',  ( 2.949999999999999734, 3.306546357697853240E-16, -2.699999999999999734 ) ) ;
#17614=VECTOR ( 'NONE', #18538, 1000.000000000000114 ) ;
#17658=TOROIDAL_SURFACE ( 'NONE', #15812, 2.699999999999999734, 0.2000000000000000111 ) ;
#17692=CARTESIAN_POINT ( 'NONE',  ( 1.560000000000000053, 0.000000000000000000, 1.500000000000000000 ) ) ;
#17711=DIRECTION ( 'NONE',  ( -1.000000000000000000, -0.000000000000000000, -0.000000000000000000 ) ) ;
#17713=CARTESIAN_POINT ( 'NONE',  ( 18.75000000000000000, 0.000000000000000000, 0.000000000000000000 ) ) ;
#17738=DIRECTION ( 'NONE',  ( 0.000000000000000000, 0.000000000000000000, 1.000000000000000000 ) ) ;
#17757=VECTOR ( 'NONE', #2135, 1000.000000000000000 ) ;
#17758=CARTESIAN_POINT ( 'NONE',  ( 2.369999999999999662, 5.817072295949927426E-16, -4.750000000000000000 ) ) ;
#17810=DIRECTION ( 'NONE',  ( 0.000000000000000000, 0.000000000000000000, 1.000000000000000000 ) ) ;
#17855=ADVANCED_FACE ( 'NONE', ( #1093 ), #12756, .T. ) ;
#17865=VERTEX_POINT ( 'NONE', #11803 ) ;
#17872=DIRECTION ( 'NONE',  ( 0.000000000000000000, 0.000000000000000000, 1.000000000000000000 ) ) ;
#17883=AXIS2_PLACEMENT_3D ( 'NONE', #3644, #4901, #3452 ) ;
#17935=VECTOR ( 'NONE', #16260, 1000.000000000000000 ) ;
#17940=CLOSED_SHELL ( 'NONE', ( #12979, #315, #9406, #7856, #1286, #8290, #13506, #12748, #18746, #10026, #18805, #17436, #5171, #1288, #7930, #9505, #12561, #7954, #17855, #9646, #11019, #13388, #9187, #5287, #294, #17439, #1617 ) ) ;
#17943=EDGE_CURVE ( 'NONE', #2106, #10362, #9611, .T. ) ;
#17988=ORIENTED_EDGE ( 'NONE', *, *, #1790, .T. ) ;
#18055=AXIS2_PLACEMENT_3D ( 'NONE', #10487, #16022, #170 ) ;
#18090=DIRECTION ( 'NONE',  ( 1.000000000000000000, 0.000000000000000000, -0.000000000000000000 ) ) ;
#18110=PRODUCT_CONTEXT ( 'NONE', #18754, 'mechanical' ) ;
#18130=DIRECTION ( 'NONE',  ( -1.000000000000000000, -0.000000000000000000, -0.000000000000000000 ) ) ;
#18169=VERTEX_POINT ( 'NONE', #12712 ) ;
#18175=AXIS2_PLACEMENT_3D ( 'NONE', #17713, #7682, #7590 ) ;
#18194=ORIENTED_EDGE ( 'NONE', *, *, #951, .F. ) ;
#18209=CARTESIAN_POINT ( 'NONE',  ( 0.000000000000000000, 0.8660254037844389297, -1.500000000000000000 ) ) ;
#18214=STYLED_ITEM ( 'NONE', ( #16652 ), #18307 ) ;
#18235=EDGE_LOOP ( 'NONE', ( #17100, #1223, #14156, #5562 ) ) ;
#18260=EDGE_LOOP ( 'NONE', ( #10771, #9914, #2764, #13057, #16533 ) ) ;
#18291=PLANE ( 'NONE',  #6872 ) ;
#18299=AXIS2_PLACEMENT_3D ( 'NONE', #14698, #17575, #3222 ) ;
#18305=ORIENTED_EDGE ( 'NONE', *, *, #1659, .F. ) ;
#18307=ADVANCED_BREP_SHAPE_REPRESENTATION ( '', ( #16636, #2030 ), #16378 ) ;
#18333=CARTESIAN_POINT ( 'NONE',  ( 0.000000000000000000, 1.732050807568878747, 7.017607234860990640E-28 ) ) ;
#18391=ORIENTED_EDGE ( 'NONE', *, *, #16392, .F. ) ;
#18401=EDGE_CURVE ( 'NONE', #8377, #3637, #193, .T. ) ;
#18405=VERTEX_POINT ( 'NONE', #9368 ) ;
#18416=CIRCLE ( 'NONE', #1321, 0.2000000000000000944 ) ;
#18433=EDGE_LOOP ( 'NONE', ( #15106, #8706 ) ) ;
#18486=ORIENTED_EDGE ( 'NONE', *, *, #18401, .T. ) ;
#18504=DIRECTION ( 'NONE',  ( 0.000000000000000000, 0.000000000000000000, 1.000000000000000000 ) ) ;
#18506=DIRECTION ( 'NONE',  ( 0.000000000000000000, -0.5000000000000003331, -0.8660254037844383745 ) ) ;
#18516=CARTESIAN_POINT ( 'NONE',  ( 1.560000000000000053, 1.732050807568878747, 7.017607234860990640E-28 ) ) ;
#18521=DIRECTION ( 'NONE',  ( -1.000000000000000000, 0.000000000000000000, 0.000000000000000000 ) ) ;
#18538=DIRECTION ( 'NONE',  ( -0.000000000000000000, -0.5000000000000003331, -0.8660254037844384856 ) ) ;
#18581=CARTESIAN_POINT ( 'NONE',  ( 1.560000000000000053, 0.8660254037844389297, 1.500000000000000000 ) ) ;
#18583=CARTESIAN_POINT ( 'NONE',  ( 1.560000000000000053, 0.000000000000000000, 0.000000000000000000 ) ) ;
#18599=CARTESIAN_POINT ( 'NONE',  ( 0.000000000000000000, 0.8660254037844389297, 1.500000000000000000 ) ) ;
#18635=DIRECTION ( 'NONE',  ( -0.000000000000000000, -0.5000000000000004441, 0.8660254037844383745 ) ) ;
#18681=EDGE_LOOP ( 'NONE', ( #4534, #18486, #14263, #14184 ) ) ;
#18684=VERTEX_POINT ( 'NONE', #13542 ) ;
#18686=DIRECTION ( 'NONE',  ( 0.000000000000000000, 0.5000000000000003331, 0.8660254037844383745 ) ) ;
#18746=ADVANCED_FACE ( 'NONE', ( #3110 ), #7732, .T. ) ;
#18754=APPLICATION_CONTEXT ( 'automotive_design' ) ;
#18762=EDGE_CURVE ( 'NONE', #12765, #7766, #10300, .T. ) ;
#18805=ADVANCED_FACE ( 'NONE', ( #13737 ), #6477, .T. ) ;
#18822=DIRECTION ( 'NONE',  ( 0.000000000000000000, 0.000000000000000000, 1.000000000000000000 ) ) ;
#18830=CARTESIAN_POINT ( 'NONE',  ( 1.560000000000000053, 0.000000000000000000, 2.999999999999998668 ) ) ;
#18841=ORIENTED_EDGE ( 'NONE', *, *, #5747, .F. ) ;
#18856=CARTESIAN_POINT ( 'NONE',  ( 1.560000000000000053, 0.000000000000000000, 0.000000000000000000 ) ) ;
#18902=AXIS2_PLACEMENT_3D ( 'NONE', #6791, #6607, #13857 ) ;
ENDSEC;
END-ISO-10303-21;
